ISO-10303-21;
HEADER;
/* Generated by software containing ST-Developer
 * from STEP Tools, Inc. (www.steptools.com) 
 */

FILE_DESCRIPTION(
/* description */ ('Worm-less right-angle friction wheel drive'),
/* implementation_level */ '2;1');

FILE_NAME(
/* name */ 'Cap Screw - M4x16.step',
/* time_stamp */ '2026-10-28T03:22:36-07:00',
/* author */ (''),
/* organization */ (''),
/* preprocessor_version */ 'ST-DEVELOPER v20.2',
/* originating_system */ 'Autodesk Translation Framework v15.17.0.0',
/* authorisation */ '');

FILE_SCHEMA (('AUTOMOTIVE_DESIGN { 1 0 10303 214 3 1 1 }'));
ENDSEC;

DATA;
#10=MECHANICAL_DESIGN_GEOMETRIC_PRESENTATION_REPRESENTATION('',(#656),#17046);
#454=ORIENTED_CLOSED_SHELL('',*,#8215,.F.);
#472=CONICAL_SURFACE('',#9542,0.325,0.785398163397448);
#473=CONICAL_SURFACE('',#9546,0.335,0.785398163397448);
#474=CONICAL_SURFACE('',#9550,0.21,0.463647609000806);
#475=CONICAL_SURFACE('',#9554,0.18,0.785398163397448);
#480=BREP_WITH_VOIDS('Body1',#8214,(#454));
#555=SHAPE_REPRESENTATION_RELATIONSHIP('SRR','None',#17300,#602);
#602=ADVANCED_BREP_SHAPE_REPRESENTATION('',(#480),#17036);
#656=STYLED_ITEM('',(#17598),#480);
#936=FACE_BOUND('',#2285,.T.);
#1151=PLANE('',#9540);
#1152=PLANE('',#9548);
#1153=PLANE('',#9556);
#1154=PLANE('',#9557);
#1155=PLANE('',#9558);
#1156=PLANE('',#9559);
#1157=PLANE('',#9560);
#1158=PLANE('',#9561);
#1159=PLANE('',#9562);
#1160=PLANE('',#9563);
#1161=PLANE('',#9564);
#1593=FACE_OUTER_BOUND('',#2280,.T.);
#1594=FACE_OUTER_BOUND('',#2281,.T.);
#1595=FACE_OUTER_BOUND('',#2282,.T.);
#1596=FACE_OUTER_BOUND('',#2283,.T.);
#1597=FACE_OUTER_BOUND('',#2284,.T.);
#1598=FACE_OUTER_BOUND('',#2286,.T.);
#1599=FACE_OUTER_BOUND('',#2287,.T.);
#1600=FACE_OUTER_BOUND('',#2288,.T.);
#1601=FACE_OUTER_BOUND('',#2289,.T.);
#1602=FACE_OUTER_BOUND('',#2290,.T.);
#1603=FACE_OUTER_BOUND('',#2291,.T.);
#1604=FACE_OUTER_BOUND('',#2292,.T.);
#1605=FACE_OUTER_BOUND('',#2293,.T.);
#1606=FACE_OUTER_BOUND('',#2294,.T.);
#1607=FACE_OUTER_BOUND('',#2295,.T.);
#1608=FACE_OUTER_BOUND('',#2296,.T.);
#1609=FACE_OUTER_BOUND('',#2297,.T.);
#2280=EDGE_LOOP('',(#7190));
#2281=EDGE_LOOP('',(#7191,#7192,#7193,#7194));
#2282=EDGE_LOOP('',(#7195,#7196,#7197,#7198));
#2283=EDGE_LOOP('',(#7199,#7200,#7201,#7202));
#2284=EDGE_LOOP('',(#7203));
#2285=EDGE_LOOP('',(#7204));
#2286=EDGE_LOOP('',(#7205,#7206,#7207,#7208));
#2287=EDGE_LOOP('',(#7209,#7210,#7211,#7212));
#2288=EDGE_LOOP('',(#7213,#7214,#7215,#7216));
#2289=EDGE_LOOP('',(#7217));
#2290=EDGE_LOOP('',(#7218,#7219,#7220,#7221));
#2291=EDGE_LOOP('',(#7222,#7223,#7224,#7225));
#2292=EDGE_LOOP('',(#7226,#7227,#7228,#7229));
#2293=EDGE_LOOP('',(#7230,#7231,#7232,#7233));
#2294=EDGE_LOOP('',(#7234,#7235,#7236,#7237));
#2295=EDGE_LOOP('',(#7238,#7239,#7240,#7241));
#2296=EDGE_LOOP('',(#7242,#7243,#7244,#7245,#7246,#7247));
#2297=EDGE_LOOP('',(#7248,#7249,#7250,#7251,#7252,#7253));
#2806=LINE('',#16368,#3346);
#2807=LINE('',#16372,#3347);
#2808=LINE('',#16376,#3348);
#2809=LINE('',#16383,#3349);
#2810=LINE('',#16387,#3350);
#2811=LINE('',#16391,#3351);
#2812=LINE('',#16396,#3352);
#2813=LINE('',#16398,#3353);
#2814=LINE('',#16400,#3354);
#2815=LINE('',#16401,#3355);
#2816=LINE('',#16404,#3356);
#2817=LINE('',#16406,#3357);
#2818=LINE('',#16407,#3358);
#2819=LINE('',#16410,#3359);
#2820=LINE('',#16412,#3360);
#2821=LINE('',#16413,#3361);
#2822=LINE('',#16416,#3362);
#2823=LINE('',#16418,#3363);
#2824=LINE('',#16419,#3364);
#2825=LINE('',#16422,#3365);
#2826=LINE('',#16424,#3366);
#2827=LINE('',#16425,#3367);
#2828=LINE('',#16427,#3368);
#2829=LINE('',#16428,#3369);
#3346=VECTOR('',#11806,0.325);
#3347=VECTOR('',#11811,0.35);
#3348=VECTOR('',#11816,0.335);
#3349=VECTOR('',#11825,0.21);
#3350=VECTOR('',#11830,0.2);
#3351=VECTOR('',#11835,0.18);
#3352=VECTOR('',#11840,1.);
#3353=VECTOR('',#11841,1.);
#3354=VECTOR('',#11842,1.);
#3355=VECTOR('',#11843,1.);
#3356=VECTOR('',#11846,1.);
#3357=VECTOR('',#11847,1.);
#3358=VECTOR('',#11848,1.);
#3359=VECTOR('',#11851,1.);
#3360=VECTOR('',#11852,1.);
#3361=VECTOR('',#11853,1.);
#3362=VECTOR('',#11856,1.);
#3363=VECTOR('',#11857,1.);
#3364=VECTOR('',#11858,1.);
#3365=VECTOR('',#11861,1.);
#3366=VECTOR('',#11862,1.);
#3367=VECTOR('',#11863,1.);
#3368=VECTOR('',#11866,1.);
#3369=VECTOR('',#11867,1.);
#3824=CIRCLE('',#9541,0.3);
#3825=CIRCLE('',#9543,0.35);
#3826=CIRCLE('',#9545,0.35);
#3827=CIRCLE('',#9547,0.32);
#3828=CIRCLE('',#9549,0.22);
#3829=CIRCLE('',#9551,0.1954);
#3830=CIRCLE('',#9553,0.1954);
#3831=CIRCLE('',#9555,0.16);
#4425=VERTEX_POINT('',#16363);
#4426=VERTEX_POINT('',#16366);
#4427=VERTEX_POINT('',#16370);
#4428=VERTEX_POINT('',#16374);
#4429=VERTEX_POINT('',#16378);
#4430=VERTEX_POINT('',#16381);
#4431=VERTEX_POINT('',#16385);
#4432=VERTEX_POINT('',#16389);
#4433=VERTEX_POINT('',#16394);
#4434=VERTEX_POINT('',#16395);
#4435=VERTEX_POINT('',#16397);
#4436=VERTEX_POINT('',#16399);
#4437=VERTEX_POINT('',#16403);
#4438=VERTEX_POINT('',#16405);
#4439=VERTEX_POINT('',#16409);
#4440=VERTEX_POINT('',#16411);
#4441=VERTEX_POINT('',#16415);
#4442=VERTEX_POINT('',#16417);
#4443=VERTEX_POINT('',#16421);
#4444=VERTEX_POINT('',#16423);
#5364=EDGE_CURVE('',#4425,#4425,#3824,.T.);
#5365=EDGE_CURVE('',#4426,#4426,#3825,.T.);
#5366=EDGE_CURVE('',#4426,#4425,#2806,.T.);
#5367=EDGE_CURVE('',#4427,#4427,#3826,.T.);
#5368=EDGE_CURVE('',#4427,#4426,#2807,.T.);
#5369=EDGE_CURVE('',#4428,#4428,#3827,.T.);
#5370=EDGE_CURVE('',#4428,#4427,#2808,.T.);
#5371=EDGE_CURVE('',#4429,#4429,#3828,.T.);
#5372=EDGE_CURVE('',#4430,#4430,#3829,.F.);
#5373=EDGE_CURVE('',#4430,#4429,#2809,.T.);
#5374=EDGE_CURVE('',#4431,#4431,#3830,.F.);
#5375=EDGE_CURVE('',#4431,#4430,#2810,.T.);
#5376=EDGE_CURVE('',#4432,#4432,#3831,.T.);
#5377=EDGE_CURVE('',#4432,#4431,#2811,.T.);
#5378=EDGE_CURVE('',#4433,#4434,#2812,.T.);
#5379=EDGE_CURVE('',#4434,#4435,#2813,.T.);
#5380=EDGE_CURVE('',#4435,#4436,#2814,.T.);
#5381=EDGE_CURVE('',#4433,#4436,#2815,.T.);
#5382=EDGE_CURVE('',#4434,#4437,#2816,.T.);
#5383=EDGE_CURVE('',#4437,#4438,#2817,.T.);
#5384=EDGE_CURVE('',#4438,#4435,#2818,.T.);
#5385=EDGE_CURVE('',#4437,#4439,#2819,.T.);
#5386=EDGE_CURVE('',#4439,#4440,#2820,.T.);
#5387=EDGE_CURVE('',#4440,#4438,#2821,.T.);
#5388=EDGE_CURVE('',#4439,#4441,#2822,.T.);
#5389=EDGE_CURVE('',#4441,#4442,#2823,.T.);
#5390=EDGE_CURVE('',#4442,#4440,#2824,.T.);
#5391=EDGE_CURVE('',#4441,#4443,#2825,.T.);
#5392=EDGE_CURVE('',#4443,#4444,#2826,.T.);
#5393=EDGE_CURVE('',#4444,#4442,#2827,.T.);
#5394=EDGE_CURVE('',#4443,#4433,#2828,.T.);
#5395=EDGE_CURVE('',#4436,#4444,#2829,.T.);
#7190=ORIENTED_EDGE('',*,*,#5364,.F.);
#7191=ORIENTED_EDGE('',*,*,#5365,.F.);
#7192=ORIENTED_EDGE('',*,*,#5366,.T.);
#7193=ORIENTED_EDGE('',*,*,#5364,.T.);
#7194=ORIENTED_EDGE('',*,*,#5366,.F.);
#7195=ORIENTED_EDGE('',*,*,#5367,.F.);
#7196=ORIENTED_EDGE('',*,*,#5368,.T.);
#7197=ORIENTED_EDGE('',*,*,#5365,.T.);
#7198=ORIENTED_EDGE('',*,*,#5368,.F.);
#7199=ORIENTED_EDGE('',*,*,#5369,.F.);
#7200=ORIENTED_EDGE('',*,*,#5370,.T.);
#7201=ORIENTED_EDGE('',*,*,#5367,.T.);
#7202=ORIENTED_EDGE('',*,*,#5370,.F.);
#7203=ORIENTED_EDGE('',*,*,#5369,.T.);
#7204=ORIENTED_EDGE('',*,*,#5371,.F.);
#7205=ORIENTED_EDGE('',*,*,#5372,.F.);
#7206=ORIENTED_EDGE('',*,*,#5373,.T.);
#7207=ORIENTED_EDGE('',*,*,#5371,.T.);
#7208=ORIENTED_EDGE('',*,*,#5373,.F.);
#7209=ORIENTED_EDGE('',*,*,#5374,.F.);
#7210=ORIENTED_EDGE('',*,*,#5375,.T.);
#7211=ORIENTED_EDGE('',*,*,#5372,.T.);
#7212=ORIENTED_EDGE('',*,*,#5375,.F.);
#7213=ORIENTED_EDGE('',*,*,#5376,.F.);
#7214=ORIENTED_EDGE('',*,*,#5377,.T.);
#7215=ORIENTED_EDGE('',*,*,#5374,.T.);
#7216=ORIENTED_EDGE('',*,*,#5377,.F.);
#7217=ORIENTED_EDGE('',*,*,#5376,.T.);
#7218=ORIENTED_EDGE('',*,*,#5378,.T.);
#7219=ORIENTED_EDGE('',*,*,#5379,.T.);
#7220=ORIENTED_EDGE('',*,*,#5380,.T.);
#7221=ORIENTED_EDGE('',*,*,#5381,.F.);
#7222=ORIENTED_EDGE('',*,*,#5382,.T.);
#7223=ORIENTED_EDGE('',*,*,#5383,.T.);
#7224=ORIENTED_EDGE('',*,*,#5384,.T.);
#7225=ORIENTED_EDGE('',*,*,#5379,.F.);
#7226=ORIENTED_EDGE('',*,*,#5385,.T.);
#7227=ORIENTED_EDGE('',*,*,#5386,.T.);
#7228=ORIENTED_EDGE('',*,*,#5387,.T.);
#7229=ORIENTED_EDGE('',*,*,#5383,.F.);
#7230=ORIENTED_EDGE('',*,*,#5388,.T.);
#7231=ORIENTED_EDGE('',*,*,#5389,.T.);
#7232=ORIENTED_EDGE('',*,*,#5390,.T.);
#7233=ORIENTED_EDGE('',*,*,#5386,.F.);
#7234=ORIENTED_EDGE('',*,*,#5391,.T.);
#7235=ORIENTED_EDGE('',*,*,#5392,.T.);
#7236=ORIENTED_EDGE('',*,*,#5393,.T.);
#7237=ORIENTED_EDGE('',*,*,#5389,.F.);
#7238=ORIENTED_EDGE('',*,*,#5394,.T.);
#7239=ORIENTED_EDGE('',*,*,#5381,.T.);
#7240=ORIENTED_EDGE('',*,*,#5395,.T.);
#7241=ORIENTED_EDGE('',*,*,#5392,.F.);
#7242=ORIENTED_EDGE('',*,*,#5394,.F.);
#7243=ORIENTED_EDGE('',*,*,#5391,.F.);
#7244=ORIENTED_EDGE('',*,*,#5388,.F.);
#7245=ORIENTED_EDGE('',*,*,#5385,.F.);
#7246=ORIENTED_EDGE('',*,*,#5382,.F.);
#7247=ORIENTED_EDGE('',*,*,#5378,.F.);
#7248=ORIENTED_EDGE('',*,*,#5395,.F.);
#7249=ORIENTED_EDGE('',*,*,#5380,.F.);
#7250=ORIENTED_EDGE('',*,*,#5384,.F.);
#7251=ORIENTED_EDGE('',*,*,#5387,.F.);
#7252=ORIENTED_EDGE('',*,*,#5390,.F.);
#7253=ORIENTED_EDGE('',*,*,#5393,.F.);
#7681=CYLINDRICAL_SURFACE('',#9544,0.35);
#7682=CYLINDRICAL_SURFACE('',#9552,0.1954);
#8085=ADVANCED_FACE('',(#1593),#1151,.T.);
#8086=ADVANCED_FACE('',(#1594),#472,.T.);
#8087=ADVANCED_FACE('',(#1595),#7681,.T.);
#8088=ADVANCED_FACE('',(#1596),#473,.T.);
#8089=ADVANCED_FACE('',(#1597,#936),#1152,.T.);
#8090=ADVANCED_FACE('',(#1598),#474,.T.);
#8091=ADVANCED_FACE('',(#1599),#7682,.T.);
#8092=ADVANCED_FACE('',(#1600),#475,.T.);
#8093=ADVANCED_FACE('',(#1601),#1153,.T.);
#8094=ADVANCED_FACE('',(#1602),#1154,.F.);
#8095=ADVANCED_FACE('',(#1603),#1155,.F.);
#8096=ADVANCED_FACE('',(#1604),#1156,.F.);
#8097=ADVANCED_FACE('',(#1605),#1157,.F.);
#8098=ADVANCED_FACE('',(#1606),#1158,.F.);
#8099=ADVANCED_FACE('',(#1607),#1159,.F.);
#8100=ADVANCED_FACE('',(#1608),#1160,.F.);
#8101=ADVANCED_FACE('',(#1609),#1161,.F.);
#8214=CLOSED_SHELL('',(#8085,#8086,#8087,#8088,#8089,#8090,#8091,#8092,
#8093));
#8215=CLOSED_SHELL('',(#8094,#8095,#8096,#8097,#8098,#8099,#8100,#8101));
#9539=AXIS2_PLACEMENT_3D('',#16361,#11796,#11797);
#9540=AXIS2_PLACEMENT_3D('',#16362,#11798,#11799);
#9541=AXIS2_PLACEMENT_3D('',#16364,#11800,#11801);
#9542=AXIS2_PLACEMENT_3D('',#16365,#11802,#11803);
#9543=AXIS2_PLACEMENT_3D('',#16367,#11804,#11805);
#9544=AXIS2_PLACEMENT_3D('',#16369,#11807,#11808);
#9545=AXIS2_PLACEMENT_3D('',#16371,#11809,#11810);
#9546=AXIS2_PLACEMENT_3D('',#16373,#11812,#11813);
#9547=AXIS2_PLACEMENT_3D('',#16375,#11814,#11815);
#9548=AXIS2_PLACEMENT_3D('',#16377,#11817,#11818);
#9549=AXIS2_PLACEMENT_3D('',#16379,#11819,#11820);
#9550=AXIS2_PLACEMENT_3D('',#16380,#11821,#11822);
#9551=AXIS2_PLACEMENT_3D('',#16382,#11823,#11824);
#9552=AXIS2_PLACEMENT_3D('',#16384,#11826,#11827);
#9553=AXIS2_PLACEMENT_3D('',#16386,#11828,#11829);
#9554=AXIS2_PLACEMENT_3D('',#16388,#11831,#11832);
#9555=AXIS2_PLACEMENT_3D('',#16390,#11833,#11834);
#9556=AXIS2_PLACEMENT_3D('',#16392,#11836,#11837);
#9557=AXIS2_PLACEMENT_3D('',#16393,#11838,#11839);
#9558=AXIS2_PLACEMENT_3D('',#16402,#11844,#11845);
#9559=AXIS2_PLACEMENT_3D('',#16408,#11849,#11850);
#9560=AXIS2_PLACEMENT_3D('',#16414,#11854,#11855);
#9561=AXIS2_PLACEMENT_3D('',#16420,#11859,#11860);
#9562=AXIS2_PLACEMENT_3D('',#16426,#11864,#11865);
#9563=AXIS2_PLACEMENT_3D('',#16429,#11868,#11869);
#9564=AXIS2_PLACEMENT_3D('',#16430,#11870,#11871);
#11796=DIRECTION('axis',(0.,0.,1.));
#11797=DIRECTION('refdir',(1.,0.,0.));
#11798=DIRECTION('center_axis',(0.,1.,0.));
#11799=DIRECTION('ref_axis',(0.,0.,1.));
#11800=DIRECTION('center_axis',(0.,-1.,0.));
#11801=DIRECTION('ref_axis',(1.,0.,0.));
#11802=DIRECTION('center_axis',(0.,-1.,0.));
#11803=DIRECTION('ref_axis',(1.,0.,0.));
#11804=DIRECTION('center_axis',(0.,-1.,0.));
#11805=DIRECTION('ref_axis',(1.,0.,0.));
#11806=DIRECTION('',(0.707106781186547,0.707106781186548,8.65956056235493E-17));
#11807=DIRECTION('center_axis',(0.,-1.,0.));
#11808=DIRECTION('ref_axis',(1.,0.,0.));
#11809=DIRECTION('center_axis',(0.,-1.,0.));
#11810=DIRECTION('ref_axis',(1.,0.,0.));
#11811=DIRECTION('',(0.,1.,0.));
#11812=DIRECTION('center_axis',(0.,1.,0.));
#11813=DIRECTION('ref_axis',(1.,0.,0.));
#11814=DIRECTION('center_axis',(0.,-1.,0.));
#11815=DIRECTION('ref_axis',(1.,0.,0.));
#11816=DIRECTION('',(-0.707106781186547,0.707106781186548,-8.65956056235493E-17));
#11817=DIRECTION('center_axis',(0.,-1.,0.));
#11818=DIRECTION('ref_axis',(0.,0.,-1.));
#11819=DIRECTION('center_axis',(0.,-1.,0.));
#11820=DIRECTION('ref_axis',(1.,0.,0.));
#11821=DIRECTION('center_axis',(0.,1.,0.));
#11822=DIRECTION('ref_axis',(1.,0.,0.));
#11823=DIRECTION('center_axis',(0.,1.,0.));
#11824=DIRECTION('ref_axis',(1.,0.,0.));
#11825=DIRECTION('',(-0.447213595499958,0.894427190999916,-5.47678698264203E-17));
#11826=DIRECTION('center_axis',(0.,-1.,0.));
#11827=DIRECTION('ref_axis',(1.,0.,0.));
#11828=DIRECTION('center_axis',(0.,1.,0.));
#11829=DIRECTION('ref_axis',(1.,0.,0.));
#11830=DIRECTION('',(0.,1.,0.));
#11831=DIRECTION('center_axis',(0.,1.,0.));
#11832=DIRECTION('ref_axis',(1.,0.,0.));
#11833=DIRECTION('center_axis',(0.,-1.,0.));
#11834=DIRECTION('ref_axis',(1.,0.,0.));
#11835=DIRECTION('',(-0.707106781186547,0.707106781186548,-8.65956056235493E-17));
#11836=DIRECTION('center_axis',(0.,-1.,0.));
#11837=DIRECTION('ref_axis',(0.,0.,-1.));
#11838=DIRECTION('center_axis',(0.866025403784439,0.,-0.5));
#11839=DIRECTION('ref_axis',(0.5,0.,0.866025403784439));
#11840=DIRECTION('',(-0.5,0.,-0.866025403784439));
#11841=DIRECTION('',(0.,-1.,0.));
#11842=DIRECTION('',(0.5,0.,0.866025403784439));
#11843=DIRECTION('',(0.,-1.,0.));
#11844=DIRECTION('center_axis',(1.60246890531964E-16,0.,-1.));
#11845=DIRECTION('ref_axis',(1.,0.,1.60246890531964E-16));
#11846=DIRECTION('',(-1.,0.,-1.60246890531964E-16));
#11847=DIRECTION('',(0.,-1.,0.));
#11848=DIRECTION('',(1.,0.,1.60246890531964E-16));
#11849=DIRECTION('center_axis',(-0.866025403784439,0.,-0.5));
#11850=DIRECTION('ref_axis',(0.5,0.,-0.866025403784439));
#11851=DIRECTION('',(-0.5,0.,0.866025403784439));
#11852=DIRECTION('',(0.,-1.,0.));
#11853=DIRECTION('',(0.5,0.,-0.866025403784439));
#11854=DIRECTION('center_axis',(-0.866025403784439,0.,0.5));
#11855=DIRECTION('ref_axis',(-0.5,0.,-0.866025403784439));
#11856=DIRECTION('',(0.5,0.,0.866025403784439));
#11857=DIRECTION('',(0.,-1.,0.));
#11858=DIRECTION('',(-0.5,0.,-0.866025403784439));
#11859=DIRECTION('center_axis',(-1.60246890531964E-16,0.,1.));
#11860=DIRECTION('ref_axis',(-1.,0.,-1.60246890531964E-16));
#11861=DIRECTION('',(1.,0.,1.60246890531964E-16));
#11862=DIRECTION('',(0.,-1.,0.));
#11863=DIRECTION('',(-1.,0.,-1.60246890531964E-16));
#11864=DIRECTION('center_axis',(0.866025403784439,0.,0.5));
#11865=DIRECTION('ref_axis',(-0.5,0.,0.866025403784439));
#11866=DIRECTION('',(0.5,0.,-0.866025403784439));
#11867=DIRECTION('',(-0.5,0.,0.866025403784439));
#11868=DIRECTION('center_axis',(0.,1.,0.));
#11869=DIRECTION('ref_axis',(1.,0.,0.));
#11870=DIRECTION('center_axis',(0.,-1.,0.));
#11871=DIRECTION('ref_axis',(0.,0.,-1.));
#16361=CARTESIAN_POINT('',(0.,0.,0.));
#16362=CARTESIAN_POINT('Origin',(0.3,0.4,0.));
#16363=CARTESIAN_POINT('',(-0.3,0.4,-3.67394039744206E-17));
#16364=CARTESIAN_POINT('Origin',(0.,0.4,0.));
#16365=CARTESIAN_POINT('Origin',(0.,0.375,0.));
#16366=CARTESIAN_POINT('',(-0.35,0.35,-4.28626379701573E-17));
#16367=CARTESIAN_POINT('Origin',(0.,0.35,0.));
#16368=CARTESIAN_POINT('',(-0.325,0.375,-3.9801020972289E-17));
#16369=CARTESIAN_POINT('Origin',(0.,0.19,0.));
#16370=CARTESIAN_POINT('',(-0.35,0.03,-4.28626379701574E-17));
#16371=CARTESIAN_POINT('Origin',(0.,0.03,0.));
#16372=CARTESIAN_POINT('',(-0.35,0.19,-4.28626379701574E-17));
#16373=CARTESIAN_POINT('Origin',(0.,0.0149999999999999,0.));
#16374=CARTESIAN_POINT('',(-0.32,-3.29597460435593E-17,-3.91886975727153E-17));
#16375=CARTESIAN_POINT('Origin',(0.,0.,0.));
#16376=CARTESIAN_POINT('',(-0.335,0.0149999999999999,-4.10256677714363E-17));
#16377=CARTESIAN_POINT('Origin',(0.22,0.,0.));
#16378=CARTESIAN_POINT('',(-0.22,-6.93889390390723E-18,-2.69422295812418E-17));
#16379=CARTESIAN_POINT('Origin',(0.,0.,0.));
#16380=CARTESIAN_POINT('Origin',(0.,-0.02,0.));
#16381=CARTESIAN_POINT('',(-0.1954,-0.0492,2.39295984553393E-17));
#16382=CARTESIAN_POINT('Origin',(0.,-0.0492,0.));
#16383=CARTESIAN_POINT('',(-0.21,-0.02,-2.57175827820944E-17));
#16384=CARTESIAN_POINT('Origin',(0.,-0.8,0.));
#16385=CARTESIAN_POINT('',(-0.1954,-1.5646,2.39295984553393E-17));
#16386=CARTESIAN_POINT('Origin',(0.,-1.5646,0.));
#16387=CARTESIAN_POINT('',(-0.1954,-0.8,-2.39295984553393E-17));
#16388=CARTESIAN_POINT('Origin',(0.,-1.58,0.));
#16389=CARTESIAN_POINT('',(-0.16,-1.6,-1.95943487863577E-17));
#16390=CARTESIAN_POINT('Origin',(0.,-1.6,0.));
#16391=CARTESIAN_POINT('',(-0.18,-1.58,-2.20436423846524E-17));
#16392=CARTESIAN_POINT('Origin',(0.,-1.6,0.));
#16393=CARTESIAN_POINT('Origin',(0.0866025403784439,-0.4,-0.15));
#16394=CARTESIAN_POINT('',(0.173205080756888,-0.4,0.));
#16395=CARTESIAN_POINT('',(0.0866025403784439,-0.4,-0.15));
#16396=CARTESIAN_POINT('',(0.173205080756888,-0.4,0.));
#16397=CARTESIAN_POINT('',(0.0866025403784439,-0.64,-0.15));
#16398=CARTESIAN_POINT('',(0.0866025403784439,-0.4,-0.15));
#16399=CARTESIAN_POINT('',(0.173205080756888,-0.64,0.));
#16400=CARTESIAN_POINT('',(0.173205080756888,-0.64,0.));
#16401=CARTESIAN_POINT('',(0.173205080756888,-0.4,0.));
#16402=CARTESIAN_POINT('Origin',(-0.0866025403784438,-0.4,-0.15));
#16403=CARTESIAN_POINT('',(-0.0866025403784438,-0.4,-0.15));
#16404=CARTESIAN_POINT('',(0.0866025403784439,-0.4,-0.15));
#16405=CARTESIAN_POINT('',(-0.0866025403784438,-0.64,-0.15));
#16406=CARTESIAN_POINT('',(-0.0866025403784438,-0.4,-0.15));
#16407=CARTESIAN_POINT('',(0.0866025403784439,-0.64,-0.15));
#16408=CARTESIAN_POINT('Origin',(-0.173205080756888,-0.4,-2.77555756156289E-17));
#16409=CARTESIAN_POINT('',(-0.173205080756888,-0.4,-2.12115047744981E-17));
#16410=CARTESIAN_POINT('',(-0.0866025403784438,-0.4,-0.15));
#16411=CARTESIAN_POINT('',(-0.173205080756888,-0.64,-2.77555756156289E-17));
#16412=CARTESIAN_POINT('',(-0.173205080756888,-0.4,-2.12115047744981E-17));
#16413=CARTESIAN_POINT('',(-0.0866025403784438,-0.64,-0.15));
#16414=CARTESIAN_POINT('Origin',(-0.0866025403784439,-0.4,0.15));
#16415=CARTESIAN_POINT('',(-0.0866025403784439,-0.4,0.15));
#16416=CARTESIAN_POINT('',(-0.173205080756888,-0.4,-2.12115047744981E-17));
#16417=CARTESIAN_POINT('',(-0.0866025403784439,-0.64,0.15));
#16418=CARTESIAN_POINT('',(-0.0866025403784439,-0.4,0.15));
#16419=CARTESIAN_POINT('',(-0.173205080756888,-0.64,-2.12115047744981E-17));
#16420=CARTESIAN_POINT('Origin',(0.0866025403784439,-0.4,0.15));
#16421=CARTESIAN_POINT('',(0.0866025403784439,-0.4,0.15));
#16422=CARTESIAN_POINT('',(-0.0866025403784439,-0.4,0.15));
#16423=CARTESIAN_POINT('',(0.0866025403784439,-0.64,0.15));
#16424=CARTESIAN_POINT('',(0.0866025403784439,-0.4,0.15));
#16425=CARTESIAN_POINT('',(-0.0866025403784439,-0.64,0.15));
#16426=CARTESIAN_POINT('Origin',(0.173205080756888,-0.4,0.));
#16427=CARTESIAN_POINT('',(0.0866025403784439,-0.4,0.15));
#16428=CARTESIAN_POINT('',(0.0866025403784439,-0.64,0.15));
#16429=CARTESIAN_POINT('Origin',(0.,-0.4,-2.77555756156289E-17));
#16430=CARTESIAN_POINT('Origin',(0.,-0.64,-2.77555756156289E-17));
#16983=UNCERTAINTY_MEASURE_WITH_UNIT(LENGTH_MEASURE(0.001),#17047,
'DISTANCE_ACCURACY_VALUE',
'Maximum model space distance between geometric entities at asserted c
onnectivities');
#16993=UNCERTAINTY_MEASURE_WITH_UNIT(LENGTH_MEASURE(0.001),#17047,
'DISTANCE_ACCURACY_VALUE',
'Maximum model space distance between geometric entities at asserted c
onnectivities');
#17036=(
GEOMETRIC_REPRESENTATION_CONTEXT(3)
GLOBAL_UNCERTAINTY_ASSIGNED_CONTEXT((#16983))
GLOBAL_UNIT_ASSIGNED_CONTEXT((#17047,#17049,#17050))
REPRESENTATION_CONTEXT('','3D')
);
#17046=(
GEOMETRIC_REPRESENTATION_CONTEXT(3)
GLOBAL_UNCERTAINTY_ASSIGNED_CONTEXT((#16993))
GLOBAL_UNIT_ASSIGNED_CONTEXT((#17047,#17049,#17050))
REPRESENTATION_CONTEXT('','3D')
);
#17047=(
LENGTH_UNIT()
NAMED_UNIT(*)
SI_UNIT(.CENTI.,.METRE.)
);
#17049=(
NAMED_UNIT(*)
PLANE_ANGLE_UNIT()
SI_UNIT($,.RADIAN.)
);
#17050=(
NAMED_UNIT(*)
SI_UNIT($,.STERADIAN.)
SOLID_ANGLE_UNIT()
);
#17093=SHAPE_DEFINITION_REPRESENTATION(#17150,#17300);
#17150=PRODUCT_DEFINITION_SHAPE('',$,#17353);
#17300=SHAPE_REPRESENTATION('',(#9539),#17036);
#17310=PRODUCT_DEFINITION_CONTEXT('part definition',#17468,'design');
#17353=PRODUCT_DEFINITION('Cap Screw - M4x16','Cap Screw - M4x16',#17405,
#17310);
#17405=PRODUCT_DEFINITION_FORMATION('',$,#17512);
#17468=APPLICATION_CONTEXT(
'Core Data for Automotive Mechanical Design Process');
#17469=PRODUCT_CONTEXT('part definition',#17468,'mechanical');
#17512=PRODUCT('Cap Screw - M4x16','Cap Screw - M4x16',
'Cap Screw - M4x16',(#17469));
#17592=COLOUR_RGB('Black',0.12,0.14,0.17);
#17593=FILL_AREA_STYLE_COLOUR('',#17592);
#17594=FILL_AREA_STYLE('',(#17593));
#17595=SURFACE_STYLE_FILL_AREA(#17594);
#17596=SURFACE_SIDE_STYLE('',(#17595));
#17597=SURFACE_STYLE_USAGE(.BOTH.,#17596);
#17598=PRESENTATION_STYLE_ASSIGNMENT((#17597));
ENDSEC;
END-ISO-10303-21;
